ISO-10303-21;
HEADER;
/* Generated by software containing ST-Developer
 * from STEP Tools, Inc. (www.steptools.com) 
 */

FILE_DESCRIPTION(
/* description */ ('Belt conveyor head drive unit'),
/* implementation_level */ '2;1');

FILE_NAME(
/* name */ 'M4x10 Cap Screw.step',
/* time_stamp */ '2026-10-28T03:26:19-07:00',
/* author */ (''),
/* organization */ (''),
/* preprocessor_version */ 'ST-DEVELOPER v20.2',
/* originating_system */ 'Autodesk Translation Framework v15.17.0.0',
/* authorisation */ '');

FILE_SCHEMA (('AUTOMOTIVE_DESIGN { 1 0 10303 214 3 1 1 }'));
ENDSEC;

DATA;
#10=MECHANICAL_DESIGN_GEOMETRIC_PRESENTATION_REPRESENTATION('',(#906),#27069);
#14=ORIENTED_CLOSED_SHELL('',*,#13774,.F.);
#19=BREP_WITH_VOIDS('Body1',#13775,(#14));
#696=CONICAL_SURFACE('',#15625,0.325,0.785398163397448);
#697=CONICAL_SURFACE('',#15629,0.335,0.785398163397448);
#698=CONICAL_SURFACE('',#15633,0.21,0.463647609000806);
#752=SHAPE_REPRESENTATION_RELATIONSHIP('SRR','None',#27399,#821);
#821=ADVANCED_BREP_SHAPE_REPRESENTATION('',(#19),#27041);
#906=STYLED_ITEM('',(#27804),#19);
#1204=FACE_BOUND('',#3137,.T.);
#1530=PLANE('',#15613);
#1531=PLANE('',#15614);
#1532=PLANE('',#15615);
#1533=PLANE('',#15616);
#1534=PLANE('',#15617);
#1535=PLANE('',#15618);
#1536=PLANE('',#15619);
#1537=PLANE('',#15620);
#1538=PLANE('',#15621);
#1539=PLANE('',#15623);
#1540=PLANE('',#15631);
#2131=FACE_OUTER_BOUND('',#3123,.T.);
#2132=FACE_OUTER_BOUND('',#3124,.T.);
#2133=FACE_OUTER_BOUND('',#3125,.T.);
#2134=FACE_OUTER_BOUND('',#3126,.T.);
#2135=FACE_OUTER_BOUND('',#3127,.T.);
#2136=FACE_OUTER_BOUND('',#3128,.T.);
#2137=FACE_OUTER_BOUND('',#3129,.T.);
#2138=FACE_OUTER_BOUND('',#3130,.T.);
#2139=FACE_OUTER_BOUND('',#3131,.T.);
#2140=FACE_OUTER_BOUND('',#3132,.T.);
#2141=FACE_OUTER_BOUND('',#3133,.T.);
#2142=FACE_OUTER_BOUND('',#3134,.T.);
#2143=FACE_OUTER_BOUND('',#3135,.T.);
#2144=FACE_OUTER_BOUND('',#3136,.T.);
#2145=FACE_OUTER_BOUND('',#3138,.T.);
#2146=FACE_OUTER_BOUND('',#3139,.T.);
#3123=EDGE_LOOP('',(#11100,#11101,#11102,#11103));
#3124=EDGE_LOOP('',(#11104,#11105,#11106,#11107));
#3125=EDGE_LOOP('',(#11108,#11109,#11110,#11111));
#3126=EDGE_LOOP('',(#11112,#11113,#11114,#11115));
#3127=EDGE_LOOP('',(#11116,#11117,#11118,#11119));
#3128=EDGE_LOOP('',(#11120,#11121,#11122,#11123));
#3129=EDGE_LOOP('',(#11124,#11125,#11126,#11127,#11128,#11129));
#3130=EDGE_LOOP('',(#11130,#11131,#11132,#11133,#11134,#11135));
#3131=EDGE_LOOP('',(#11136));
#3132=EDGE_LOOP('',(#11137));
#3133=EDGE_LOOP('',(#11138,#11139,#11140,#11141));
#3134=EDGE_LOOP('',(#11142,#11143,#11144,#11145));
#3135=EDGE_LOOP('',(#11146,#11147,#11148,#11149));
#3136=EDGE_LOOP('',(#11150));
#3137=EDGE_LOOP('',(#11151));
#3138=EDGE_LOOP('',(#11152,#11153,#11154,#11155));
#3139=EDGE_LOOP('',(#11156,#11157,#11158,#11159));
#4021=LINE('',#24378,#4813);
#4022=LINE('',#24380,#4814);
#4023=LINE('',#24382,#4815);
#4024=LINE('',#24383,#4816);
#4025=LINE('',#24386,#4817);
#4026=LINE('',#24388,#4818);
#4027=LINE('',#24389,#4819);
#4028=LINE('',#24392,#4820);
#4029=LINE('',#24394,#4821);
#4030=LINE('',#24395,#4822);
#4031=LINE('',#24398,#4823);
#4032=LINE('',#24400,#4824);
#4033=LINE('',#24401,#4825);
#4034=LINE('',#24404,#4826);
#4035=LINE('',#24406,#4827);
#4036=LINE('',#24407,#4828);
#4037=LINE('',#24409,#4829);
#4038=LINE('',#24410,#4830);
#4039=LINE('',#24422,#4831);
#4040=LINE('',#24426,#4832);
#4041=LINE('',#24430,#4833);
#4042=LINE('',#24437,#4834);
#4043=LINE('',#24439,#4835);
#4813=VECTOR('',#19061,1.);
#4814=VECTOR('',#19062,1.);
#4815=VECTOR('',#19063,1.);
#4816=VECTOR('',#19064,1.);
#4817=VECTOR('',#19067,1.);
#4818=VECTOR('',#19068,1.);
#4819=VECTOR('',#19069,1.);
#4820=VECTOR('',#19072,1.);
#4821=VECTOR('',#19073,1.);
#4822=VECTOR('',#19074,1.);
#4823=VECTOR('',#19077,1.);
#4824=VECTOR('',#19078,1.);
#4825=VECTOR('',#19079,1.);
#4826=VECTOR('',#19082,1.);
#4827=VECTOR('',#19083,1.);
#4828=VECTOR('',#19084,1.);
#4829=VECTOR('',#19087,1.);
#4830=VECTOR('',#19088,1.);
#4831=VECTOR('',#19105,0.325);
#4832=VECTOR('',#19110,0.35);
#4833=VECTOR('',#19115,0.335);
#4834=VECTOR('',#19124,0.21);
#4835=VECTOR('',#19127,0.2);
#5574=CIRCLE('',#15622,0.1954);
#5575=CIRCLE('',#15624,0.3);
#5576=CIRCLE('',#15626,0.35);
#5577=CIRCLE('',#15628,0.35);
#5578=CIRCLE('',#15630,0.32);
#5579=CIRCLE('',#15632,0.22);
#5580=CIRCLE('',#15634,0.1954);
#6688=VERTEX_POINT('',#24376);
#6689=VERTEX_POINT('',#24377);
#6690=VERTEX_POINT('',#24379);
#6691=VERTEX_POINT('',#24381);
#6692=VERTEX_POINT('',#24385);
#6693=VERTEX_POINT('',#24387);
#6694=VERTEX_POINT('',#24391);
#6695=VERTEX_POINT('',#24393);
#6696=VERTEX_POINT('',#24397);
#6697=VERTEX_POINT('',#24399);
#6698=VERTEX_POINT('',#24403);
#6699=VERTEX_POINT('',#24405);
#6700=VERTEX_POINT('',#24414);
#6701=VERTEX_POINT('',#24417);
#6702=VERTEX_POINT('',#24420);
#6703=VERTEX_POINT('',#24424);
#6704=VERTEX_POINT('',#24428);
#6705=VERTEX_POINT('',#24432);
#6706=VERTEX_POINT('',#24435);
#8242=EDGE_CURVE('',#6688,#6689,#4021,.T.);
#8243=EDGE_CURVE('',#6689,#6690,#4022,.T.);
#8244=EDGE_CURVE('',#6690,#6691,#4023,.T.);
#8245=EDGE_CURVE('',#6688,#6691,#4024,.T.);
#8246=EDGE_CURVE('',#6689,#6692,#4025,.T.);
#8247=EDGE_CURVE('',#6692,#6693,#4026,.T.);
#8248=EDGE_CURVE('',#6693,#6690,#4027,.T.);
#8249=EDGE_CURVE('',#6692,#6694,#4028,.T.);
#8250=EDGE_CURVE('',#6694,#6695,#4029,.T.);
#8251=EDGE_CURVE('',#6695,#6693,#4030,.T.);
#8252=EDGE_CURVE('',#6694,#6696,#4031,.T.);
#8253=EDGE_CURVE('',#6696,#6697,#4032,.T.);
#8254=EDGE_CURVE('',#6697,#6695,#4033,.T.);
#8255=EDGE_CURVE('',#6696,#6698,#4034,.T.);
#8256=EDGE_CURVE('',#6698,#6699,#4035,.T.);
#8257=EDGE_CURVE('',#6699,#6697,#4036,.T.);
#8258=EDGE_CURVE('',#6698,#6688,#4037,.T.);
#8259=EDGE_CURVE('',#6691,#6699,#4038,.T.);
#8260=EDGE_CURVE('',#6700,#6700,#5574,.T.);
#8261=EDGE_CURVE('',#6701,#6701,#5575,.T.);
#8262=EDGE_CURVE('',#6702,#6702,#5576,.T.);
#8263=EDGE_CURVE('',#6702,#6701,#4039,.T.);
#8264=EDGE_CURVE('',#6703,#6703,#5577,.T.);
#8265=EDGE_CURVE('',#6703,#6702,#4040,.T.);
#8266=EDGE_CURVE('',#6704,#6704,#5578,.T.);
#8267=EDGE_CURVE('',#6704,#6703,#4041,.T.);
#8268=EDGE_CURVE('',#6705,#6705,#5579,.T.);
#8269=EDGE_CURVE('',#6706,#6706,#5580,.F.);
#8270=EDGE_CURVE('',#6706,#6705,#4042,.T.);
#8271=EDGE_CURVE('',#6700,#6706,#4043,.T.);
#11100=ORIENTED_EDGE('',*,*,#8242,.T.);
#11101=ORIENTED_EDGE('',*,*,#8243,.T.);
#11102=ORIENTED_EDGE('',*,*,#8244,.T.);
#11103=ORIENTED_EDGE('',*,*,#8245,.F.);
#11104=ORIENTED_EDGE('',*,*,#8246,.T.);
#11105=ORIENTED_EDGE('',*,*,#8247,.T.);
#11106=ORIENTED_EDGE('',*,*,#8248,.T.);
#11107=ORIENTED_EDGE('',*,*,#8243,.F.);
#11108=ORIENTED_EDGE('',*,*,#8249,.T.);
#11109=ORIENTED_EDGE('',*,*,#8250,.T.);
#11110=ORIENTED_EDGE('',*,*,#8251,.T.);
#11111=ORIENTED_EDGE('',*,*,#8247,.F.);
#11112=ORIENTED_EDGE('',*,*,#8252,.T.);
#11113=ORIENTED_EDGE('',*,*,#8253,.T.);
#11114=ORIENTED_EDGE('',*,*,#8254,.T.);
#11115=ORIENTED_EDGE('',*,*,#8250,.F.);
#11116=ORIENTED_EDGE('',*,*,#8255,.T.);
#11117=ORIENTED_EDGE('',*,*,#8256,.T.);
#11118=ORIENTED_EDGE('',*,*,#8257,.T.);
#11119=ORIENTED_EDGE('',*,*,#8253,.F.);
#11120=ORIENTED_EDGE('',*,*,#8258,.T.);
#11121=ORIENTED_EDGE('',*,*,#8245,.T.);
#11122=ORIENTED_EDGE('',*,*,#8259,.T.);
#11123=ORIENTED_EDGE('',*,*,#8256,.F.);
#11124=ORIENTED_EDGE('',*,*,#8258,.F.);
#11125=ORIENTED_EDGE('',*,*,#8255,.F.);
#11126=ORIENTED_EDGE('',*,*,#8252,.F.);
#11127=ORIENTED_EDGE('',*,*,#8249,.F.);
#11128=ORIENTED_EDGE('',*,*,#8246,.F.);
#11129=ORIENTED_EDGE('',*,*,#8242,.F.);
#11130=ORIENTED_EDGE('',*,*,#8259,.F.);
#11131=ORIENTED_EDGE('',*,*,#8244,.F.);
#11132=ORIENTED_EDGE('',*,*,#8248,.F.);
#11133=ORIENTED_EDGE('',*,*,#8251,.F.);
#11134=ORIENTED_EDGE('',*,*,#8254,.F.);
#11135=ORIENTED_EDGE('',*,*,#8257,.F.);
#11136=ORIENTED_EDGE('',*,*,#8260,.F.);
#11137=ORIENTED_EDGE('',*,*,#8261,.F.);
#11138=ORIENTED_EDGE('',*,*,#8262,.F.);
#11139=ORIENTED_EDGE('',*,*,#8263,.T.);
#11140=ORIENTED_EDGE('',*,*,#8261,.T.);
#11141=ORIENTED_EDGE('',*,*,#8263,.F.);
#11142=ORIENTED_EDGE('',*,*,#8264,.F.);
#11143=ORIENTED_EDGE('',*,*,#8265,.T.);
#11144=ORIENTED_EDGE('',*,*,#8262,.T.);
#11145=ORIENTED_EDGE('',*,*,#8265,.F.);
#11146=ORIENTED_EDGE('',*,*,#8266,.F.);
#11147=ORIENTED_EDGE('',*,*,#8267,.T.);
#11148=ORIENTED_EDGE('',*,*,#8264,.T.);
#11149=ORIENTED_EDGE('',*,*,#8267,.F.);
#11150=ORIENTED_EDGE('',*,*,#8266,.T.);
#11151=ORIENTED_EDGE('',*,*,#8268,.F.);
#11152=ORIENTED_EDGE('',*,*,#8269,.F.);
#11153=ORIENTED_EDGE('',*,*,#8270,.T.);
#11154=ORIENTED_EDGE('',*,*,#8268,.T.);
#11155=ORIENTED_EDGE('',*,*,#8270,.F.);
#11156=ORIENTED_EDGE('',*,*,#8260,.T.);
#11157=ORIENTED_EDGE('',*,*,#8271,.T.);
#11158=ORIENTED_EDGE('',*,*,#8269,.T.);
#11159=ORIENTED_EDGE('',*,*,#8271,.F.);
#12722=CYLINDRICAL_SURFACE('',#15627,0.35);
#12723=CYLINDRICAL_SURFACE('',#15635,0.1954);
#13410=ADVANCED_FACE('',(#2131),#1530,.F.);
#13411=ADVANCED_FACE('',(#2132),#1531,.F.);
#13412=ADVANCED_FACE('',(#2133),#1532,.F.);
#13413=ADVANCED_FACE('',(#2134),#1533,.F.);
#13414=ADVANCED_FACE('',(#2135),#1534,.F.);
#13415=ADVANCED_FACE('',(#2136),#1535,.F.);
#13416=ADVANCED_FACE('',(#2137),#1536,.F.);
#13417=ADVANCED_FACE('',(#2138),#1537,.F.);
#13418=ADVANCED_FACE('',(#2139),#1538,.F.);
#13419=ADVANCED_FACE('',(#2140),#1539,.T.);
#13420=ADVANCED_FACE('',(#2141),#696,.T.);
#13421=ADVANCED_FACE('',(#2142),#12722,.T.);
#13422=ADVANCED_FACE('',(#2143),#697,.T.);
#13423=ADVANCED_FACE('',(#2144,#1204),#1540,.T.);
#13424=ADVANCED_FACE('',(#2145),#698,.T.);
#13425=ADVANCED_FACE('',(#2146),#12723,.T.);
#13774=CLOSED_SHELL('',(#13410,#13411,#13412,#13413,#13414,#13415,#13416,
#13417));
#13775=CLOSED_SHELL('',(#13418,#13419,#13420,#13421,#13422,#13423,#13424,
#13425));
#15612=AXIS2_PLACEMENT_3D('',#24374,#19057,#19058);
#15613=AXIS2_PLACEMENT_3D('',#24375,#19059,#19060);
#15614=AXIS2_PLACEMENT_3D('',#24384,#19065,#19066);
#15615=AXIS2_PLACEMENT_3D('',#24390,#19070,#19071);
#15616=AXIS2_PLACEMENT_3D('',#24396,#19075,#19076);
#15617=AXIS2_PLACEMENT_3D('',#24402,#19080,#19081);
#15618=AXIS2_PLACEMENT_3D('',#24408,#19085,#19086);
#15619=AXIS2_PLACEMENT_3D('',#24411,#19089,#19090);
#15620=AXIS2_PLACEMENT_3D('',#24412,#19091,#19092);
#15621=AXIS2_PLACEMENT_3D('',#24413,#19093,#19094);
#15622=AXIS2_PLACEMENT_3D('',#24415,#19095,#19096);
#15623=AXIS2_PLACEMENT_3D('',#24416,#19097,#19098);
#15624=AXIS2_PLACEMENT_3D('',#24418,#19099,#19100);
#15625=AXIS2_PLACEMENT_3D('',#24419,#19101,#19102);
#15626=AXIS2_PLACEMENT_3D('',#24421,#19103,#19104);
#15627=AXIS2_PLACEMENT_3D('',#24423,#19106,#19107);
#15628=AXIS2_PLACEMENT_3D('',#24425,#19108,#19109);
#15629=AXIS2_PLACEMENT_3D('',#24427,#19111,#19112);
#15630=AXIS2_PLACEMENT_3D('',#24429,#19113,#19114);
#15631=AXIS2_PLACEMENT_3D('',#24431,#19116,#19117);
#15632=AXIS2_PLACEMENT_3D('',#24433,#19118,#19119);
#15633=AXIS2_PLACEMENT_3D('',#24434,#19120,#19121);
#15634=AXIS2_PLACEMENT_3D('',#24436,#19122,#19123);
#15635=AXIS2_PLACEMENT_3D('',#24438,#19125,#19126);
#19057=DIRECTION('axis',(0.,0.,1.));
#19058=DIRECTION('refdir',(1.,0.,0.));
#19059=DIRECTION('center_axis',(0.866025403784439,0.,-0.5));
#19060=DIRECTION('ref_axis',(0.5,0.,0.866025403784439));
#19061=DIRECTION('',(-0.5,0.,-0.866025403784439));
#19062=DIRECTION('',(0.,-1.,0.));
#19063=DIRECTION('',(0.5,0.,0.866025403784439));
#19064=DIRECTION('',(0.,-1.,0.));
#19065=DIRECTION('center_axis',(1.60246890531964E-16,0.,-1.));
#19066=DIRECTION('ref_axis',(1.,0.,1.60246890531964E-16));
#19067=DIRECTION('',(-1.,0.,-1.60246890531964E-16));
#19068=DIRECTION('',(0.,-1.,0.));
#19069=DIRECTION('',(1.,0.,1.60246890531964E-16));
#19070=DIRECTION('center_axis',(-0.866025403784439,0.,-0.5));
#19071=DIRECTION('ref_axis',(0.5,0.,-0.866025403784439));
#19072=DIRECTION('',(-0.5,0.,0.866025403784439));
#19073=DIRECTION('',(0.,-1.,0.));
#19074=DIRECTION('',(0.5,0.,-0.866025403784439));
#19075=DIRECTION('center_axis',(-0.866025403784439,0.,0.5));
#19076=DIRECTION('ref_axis',(-0.5,0.,-0.866025403784439));
#19077=DIRECTION('',(0.5,0.,0.866025403784439));
#19078=DIRECTION('',(0.,-1.,0.));
#19079=DIRECTION('',(-0.5,0.,-0.866025403784439));
#19080=DIRECTION('center_axis',(-1.60246890531964E-16,0.,1.));
#19081=DIRECTION('ref_axis',(-1.,0.,-1.60246890531964E-16));
#19082=DIRECTION('',(1.,0.,1.60246890531964E-16));
#19083=DIRECTION('',(0.,-1.,0.));
#19084=DIRECTION('',(-1.,0.,-1.60246890531964E-16));
#19085=DIRECTION('center_axis',(0.866025403784439,0.,0.5));
#19086=DIRECTION('ref_axis',(-0.5,0.,0.866025403784439));
#19087=DIRECTION('',(0.5,0.,-0.866025403784439));
#19088=DIRECTION('',(-0.5,0.,0.866025403784439));
#19089=DIRECTION('center_axis',(0.,1.,0.));
#19090=DIRECTION('ref_axis',(1.,0.,0.));
#19091=DIRECTION('center_axis',(0.,-1.,0.));
#19092=DIRECTION('ref_axis',(0.,0.,-1.));
#19093=DIRECTION('center_axis',(0.,1.,0.));
#19094=DIRECTION('ref_axis',(1.,0.,0.));
#19095=DIRECTION('center_axis',(0.,1.,0.));
#19096=DIRECTION('ref_axis',(1.,0.,0.));
#19097=DIRECTION('center_axis',(0.,1.,0.));
#19098=DIRECTION('ref_axis',(0.,0.,1.));
#19099=DIRECTION('center_axis',(0.,-1.,0.));
#19100=DIRECTION('ref_axis',(1.,0.,0.));
#19101=DIRECTION('center_axis',(0.,-1.,0.));
#19102=DIRECTION('ref_axis',(1.,0.,0.));
#19103=DIRECTION('center_axis',(0.,-1.,0.));
#19104=DIRECTION('ref_axis',(1.,0.,0.));
#19105=DIRECTION('',(0.707106781186547,0.707106781186548,8.65956056235493E-17));
#19106=DIRECTION('center_axis',(0.,-1.,0.));
#19107=DIRECTION('ref_axis',(1.,0.,0.));
#19108=DIRECTION('center_axis',(0.,-1.,0.));
#19109=DIRECTION('ref_axis',(1.,0.,0.));
#19110=DIRECTION('',(0.,1.,0.));
#19111=DIRECTION('center_axis',(0.,1.,0.));
#19112=DIRECTION('ref_axis',(1.,0.,0.));
#19113=DIRECTION('center_axis',(0.,-1.,0.));
#19114=DIRECTION('ref_axis',(1.,0.,0.));
#19115=DIRECTION('',(-0.707106781186547,0.707106781186548,-8.65956056235493E-17));
#19116=DIRECTION('center_axis',(0.,-1.,0.));
#19117=DIRECTION('ref_axis',(0.,0.,-1.));
#19118=DIRECTION('center_axis',(0.,-1.,0.));
#19119=DIRECTION('ref_axis',(1.,0.,0.));
#19120=DIRECTION('center_axis',(0.,1.,0.));
#19121=DIRECTION('ref_axis',(1.,0.,0.));
#19122=DIRECTION('center_axis',(0.,1.,0.));
#19123=DIRECTION('ref_axis',(1.,0.,0.));
#19124=DIRECTION('',(-0.447213595499958,0.894427190999916,-5.47678698264203E-17));
#19125=DIRECTION('center_axis',(0.,-1.,0.));
#19126=DIRECTION('ref_axis',(1.,0.,0.));
#19127=DIRECTION('',(0.,1.,0.));
#24374=CARTESIAN_POINT('',(0.,0.,0.));
#24375=CARTESIAN_POINT('Origin',(0.0866025403784439,-0.4,-0.15));
#24376=CARTESIAN_POINT('',(0.173205080756888,-0.4,0.));
#24377=CARTESIAN_POINT('',(0.0866025403784439,-0.4,-0.15));
#24378=CARTESIAN_POINT('',(0.173205080756888,-0.4,0.));
#24379=CARTESIAN_POINT('',(0.0866025403784439,-0.64,-0.15));
#24380=CARTESIAN_POINT('',(0.0866025403784439,-0.4,-0.15));
#24381=CARTESIAN_POINT('',(0.173205080756888,-0.64,0.));
#24382=CARTESIAN_POINT('',(0.173205080756888,-0.64,0.));
#24383=CARTESIAN_POINT('',(0.173205080756888,-0.4,0.));
#24384=CARTESIAN_POINT('Origin',(-0.0866025403784438,-0.4,-0.15));
#24385=CARTESIAN_POINT('',(-0.0866025403784438,-0.4,-0.15));
#24386=CARTESIAN_POINT('',(0.0866025403784439,-0.4,-0.15));
#24387=CARTESIAN_POINT('',(-0.0866025403784438,-0.64,-0.15));
#24388=CARTESIAN_POINT('',(-0.0866025403784438,-0.4,-0.15));
#24389=CARTESIAN_POINT('',(0.0866025403784439,-0.64,-0.15));
#24390=CARTESIAN_POINT('Origin',(-0.173205080756888,-0.4,-2.77555756156289E-17));
#24391=CARTESIAN_POINT('',(-0.173205080756888,-0.4,-2.12115047744981E-17));
#24392=CARTESIAN_POINT('',(-0.0866025403784438,-0.4,-0.15));
#24393=CARTESIAN_POINT('',(-0.173205080756888,-0.64,-2.77555756156289E-17));
#24394=CARTESIAN_POINT('',(-0.173205080756888,-0.4,-2.12115047744981E-17));
#24395=CARTESIAN_POINT('',(-0.0866025403784438,-0.64,-0.15));
#24396=CARTESIAN_POINT('Origin',(-0.0866025403784439,-0.4,0.15));
#24397=CARTESIAN_POINT('',(-0.0866025403784439,-0.4,0.15));
#24398=CARTESIAN_POINT('',(-0.173205080756888,-0.4,-2.12115047744981E-17));
#24399=CARTESIAN_POINT('',(-0.0866025403784439,-0.64,0.15));
#24400=CARTESIAN_POINT('',(-0.0866025403784439,-0.4,0.15));
#24401=CARTESIAN_POINT('',(-0.173205080756888,-0.64,-2.12115047744981E-17));
#24402=CARTESIAN_POINT('Origin',(0.0866025403784439,-0.4,0.15));
#24403=CARTESIAN_POINT('',(0.0866025403784439,-0.4,0.15));
#24404=CARTESIAN_POINT('',(-0.0866025403784439,-0.4,0.15));
#24405=CARTESIAN_POINT('',(0.0866025403784439,-0.64,0.15));
#24406=CARTESIAN_POINT('',(0.0866025403784439,-0.4,0.15));
#24407=CARTESIAN_POINT('',(-0.0866025403784439,-0.64,0.15));
#24408=CARTESIAN_POINT('Origin',(0.173205080756888,-0.4,0.));
#24409=CARTESIAN_POINT('',(0.0866025403784439,-0.4,0.15));
#24410=CARTESIAN_POINT('',(0.0866025403784439,-0.64,0.15));
#24411=CARTESIAN_POINT('Origin',(0.,-0.4,-2.77555756156289E-17));
#24412=CARTESIAN_POINT('Origin',(0.,-0.64,-2.77555756156289E-17));
#24413=CARTESIAN_POINT('Origin',(0.,-1.,0.));
#24414=CARTESIAN_POINT('',(-0.1954,-1.,2.39295984553393E-17));
#24415=CARTESIAN_POINT('Origin',(0.,-1.,0.));
#24416=CARTESIAN_POINT('Origin',(0.3,0.4,0.));
#24417=CARTESIAN_POINT('',(-0.3,0.4,-3.67394039744206E-17));
#24418=CARTESIAN_POINT('Origin',(0.,0.4,0.));
#24419=CARTESIAN_POINT('Origin',(0.,0.375,0.));
#24420=CARTESIAN_POINT('',(-0.35,0.35,-4.28626379701573E-17));
#24421=CARTESIAN_POINT('Origin',(0.,0.35,0.));
#24422=CARTESIAN_POINT('',(-0.325,0.375,-3.9801020972289E-17));
#24423=CARTESIAN_POINT('Origin',(0.,0.19,0.));
#24424=CARTESIAN_POINT('',(-0.35,0.03,-4.28626379701574E-17));
#24425=CARTESIAN_POINT('Origin',(0.,0.03,0.));
#24426=CARTESIAN_POINT('',(-0.35,0.19,-4.28626379701574E-17));
#24427=CARTESIAN_POINT('Origin',(0.,0.0149999999999999,0.));
#24428=CARTESIAN_POINT('',(-0.32,-3.29597460435593E-17,-3.91886975727153E-17));
#24429=CARTESIAN_POINT('Origin',(0.,0.,0.));
#24430=CARTESIAN_POINT('',(-0.335,0.0149999999999999,-4.10256677714363E-17));
#24431=CARTESIAN_POINT('Origin',(0.22,0.,0.));
#24432=CARTESIAN_POINT('',(-0.22,-6.93889390390723E-18,-2.69422295812418E-17));
#24433=CARTESIAN_POINT('Origin',(0.,0.,0.));
#24434=CARTESIAN_POINT('Origin',(0.,-0.02,0.));
#24435=CARTESIAN_POINT('',(-0.1954,-0.0492,2.39295984553393E-17));
#24436=CARTESIAN_POINT('Origin',(0.,-0.0492,0.));
#24437=CARTESIAN_POINT('',(-0.21,-0.02,-2.57175827820944E-17));
#24438=CARTESIAN_POINT('Origin',(0.,-0.8,0.));
#24439=CARTESIAN_POINT('',(-0.1954,-0.8,-2.39295984553393E-17));
#26964=UNCERTAINTY_MEASURE_WITH_UNIT(LENGTH_MEASURE(0.001),#27070,
'DISTANCE_ACCURACY_VALUE',
'Maximum model space distance between geometric entities at asserted c
onnectivities');
#26992=UNCERTAINTY_MEASURE_WITH_UNIT(LENGTH_MEASURE(0.001),#27070,
'DISTANCE_ACCURACY_VALUE',
'Maximum model space distance between geometric entities at asserted c
onnectivities');
#27041=(
GEOMETRIC_REPRESENTATION_CONTEXT(3)
GLOBAL_UNCERTAINTY_ASSIGNED_CONTEXT((#26964))
GLOBAL_UNIT_ASSIGNED_CONTEXT((#27070,#27072,#27073))
REPRESENTATION_CONTEXT('','3D')
);
#27069=(
GEOMETRIC_REPRESENTATION_CONTEXT(3)
GLOBAL_UNCERTAINTY_ASSIGNED_CONTEXT((#26992))
GLOBAL_UNIT_ASSIGNED_CONTEXT((#27070,#27072,#27073))
REPRESENTATION_CONTEXT('','3D')
);
#27070=(
LENGTH_UNIT()
NAMED_UNIT(*)
SI_UNIT(.CENTI.,.METRE.)
);
#27072=(
NAMED_UNIT(*)
PLANE_ANGLE_UNIT()
SI_UNIT($,.RADIAN.)
);
#27073=(
NAMED_UNIT(*)
SI_UNIT($,.STERADIAN.)
SOLID_ANGLE_UNIT()
);
#27122=SHAPE_DEFINITION_REPRESENTATION(#27210,#27399);
#27210=PRODUCT_DEFINITION_SHAPE('',$,#27476);
#27399=SHAPE_REPRESENTATION('',(#15612),#27041);
#27427=PRODUCT_DEFINITION_CONTEXT('part definition',#27657,'design');
#27476=PRODUCT_DEFINITION('M4x10 Cap Screw','M4x10 Cap Screw',#27552,#27427);
#27552=PRODUCT_DEFINITION_FORMATION('',$,#27707);
#27657=APPLICATION_CONTEXT(
'Core Data for Automotive Mechanical Design Process');
#27658=PRODUCT_CONTEXT('part definition',#27657,'mechanical');
#27707=PRODUCT('M4x10 Cap Screw','M4x10 Cap Screw','M4x10 Cap Screw',(#27658));
#27798=COLOUR_RGB('Black',0.12,0.14,0.17);
#27799=FILL_AREA_STYLE_COLOUR('',#27798);
#27800=FILL_AREA_STYLE('',(#27799));
#27801=SURFACE_STYLE_FILL_AREA(#27800);
#27802=SURFACE_SIDE_STYLE('',(#27801));
#27803=SURFACE_STYLE_USAGE(.BOTH.,#27802);
#27804=PRESENTATION_STYLE_ASSIGNMENT((#27803));
ENDSEC;
END-ISO-10303-21;
